ISO-10303-21;
HEADER;
/* Generated by software containing ST-Developer
 * from STEP Tools, Inc. (www.steptools.com) 
 */

FILE_DESCRIPTION(
/* description */ ('STEP AP214'),
/* implementation_level */ '2;1');

FILE_NAME(
/* name */ 'Ball Screw Support Plate.step',
/* time_stamp */ '2026-11-15T14:55:55-08:00',
/* author */ (''),
/* organization */ (''),
/* preprocessor_version */ 'ST-DEVELOPER v20.2',
/* originating_system */ 'Autodesk Translation Framework v15.17.0.0',
/* authorisation */ '');

FILE_SCHEMA (('AUTOMOTIVE_DESIGN { 1 0 10303 214 3 1 1 }'));
ENDSEC;

DATA;
#10=MECHANICAL_DESIGN_GEOMETRIC_PRESENTATION_REPRESENTATION('',(#945),#57079);
#885=SHAPE_REPRESENTATION_RELATIONSHIP('SRR','None',#57274,#914);
#914=ADVANCED_BREP_SHAPE_REPRESENTATION('',(#982),#57066);
#945=STYLED_ITEM('',(#57444),#982);
#982=MANIFOLD_SOLID_BREP('Body1',#24545);
#1171=FACE_BOUND('',#4359,.T.);
#1172=FACE_BOUND('',#4360,.T.);
#1173=FACE_BOUND('',#4361,.T.);
#1174=FACE_BOUND('',#4362,.T.);
#1175=FACE_BOUND('',#4363,.T.);
#1176=FACE_BOUND('',#4364,.T.);
#1177=FACE_BOUND('',#4366,.T.);
#1178=FACE_BOUND('',#4367,.T.);
#1179=FACE_BOUND('',#4368,.T.);
#1180=FACE_BOUND('',#4369,.T.);
#1181=FACE_BOUND('',#4370,.T.);
#1182=FACE_BOUND('',#4371,.T.);
#1668=PLANE('',#26035);
#1669=PLANE('',#26036);
#1670=PLANE('',#26037);
#1671=PLANE('',#26038);
#1672=PLANE('',#26039);
#1673=PLANE('',#26040);
#2802=FACE_OUTER_BOUND('',#4348,.T.);
#2803=FACE_OUTER_BOUND('',#4349,.T.);
#2804=FACE_OUTER_BOUND('',#4350,.T.);
#2805=FACE_OUTER_BOUND('',#4351,.T.);
#2806=FACE_OUTER_BOUND('',#4352,.T.);
#2807=FACE_OUTER_BOUND('',#4353,.T.);
#2808=FACE_OUTER_BOUND('',#4354,.T.);
#2809=FACE_OUTER_BOUND('',#4355,.T.);
#2810=FACE_OUTER_BOUND('',#4356,.T.);
#2811=FACE_OUTER_BOUND('',#4357,.T.);
#2812=FACE_OUTER_BOUND('',#4358,.T.);
#2813=FACE_OUTER_BOUND('',#4365,.T.);
#4348=EDGE_LOOP('',(#18952,#18953,#18954,#18955));
#4349=EDGE_LOOP('',(#18956,#18957,#18958,#18959));
#4350=EDGE_LOOP('',(#18960,#18961,#18962,#18963));
#4351=EDGE_LOOP('',(#18964,#18965,#18966,#18967));
#4352=EDGE_LOOP('',(#18968,#18969,#18970,#18971));
#4353=EDGE_LOOP('',(#18972,#18973,#18974,#18975));
#4354=EDGE_LOOP('',(#18976,#18977,#18978,#18979));
#4355=EDGE_LOOP('',(#18980,#18981,#18982,#18983));
#4356=EDGE_LOOP('',(#18984,#18985,#18986,#18987));
#4357=EDGE_LOOP('',(#18988,#18989,#18990,#18991));
#4358=EDGE_LOOP('',(#18992,#18993,#18994,#18995));
#4359=EDGE_LOOP('',(#18996));
#4360=EDGE_LOOP('',(#18997));
#4361=EDGE_LOOP('',(#18998));
#4362=EDGE_LOOP('',(#18999));
#4363=EDGE_LOOP('',(#19000));
#4364=EDGE_LOOP('',(#19001));
#4365=EDGE_LOOP('',(#19002,#19003,#19004,#19005));
#4366=EDGE_LOOP('',(#19006));
#4367=EDGE_LOOP('',(#19007));
#4368=EDGE_LOOP('',(#19008));
#4369=EDGE_LOOP('',(#19009));
#4370=EDGE_LOOP('',(#19010));
#4371=EDGE_LOOP('',(#19011));
#5999=LINE('',#52864,#7966);
#6000=LINE('',#52870,#7967);
#6001=LINE('',#52876,#7968);
#6002=LINE('',#52882,#7969);
#6003=LINE('',#52888,#7970);
#6004=LINE('',#52894,#7971);
#6005=LINE('',#52899,#7972);
#6006=LINE('',#52901,#7973);
#6007=LINE('',#52903,#7974);
#6008=LINE('',#52904,#7975);
#6009=LINE('',#52907,#7976);
#6010=LINE('',#52909,#7977);
#6011=LINE('',#52910,#7978);
#6012=LINE('',#52913,#7979);
#6013=LINE('',#52915,#7980);
#6014=LINE('',#52916,#7981);
#6015=LINE('',#52918,#7982);
#6016=LINE('',#52919,#7983);
#7966=VECTOR('',#30497,2.99999999999999);
#7967=VECTOR('',#30504,2.99999999999999);
#7968=VECTOR('',#30511,3.3);
#7969=VECTOR('',#30518,3.3);
#7970=VECTOR('',#30525,3.3);
#7971=VECTOR('',#30532,3.3);
#7972=VECTOR('',#30537,1000.);
#7973=VECTOR('',#30538,1000.);
#7974=VECTOR('',#30539,1000.);
#7975=VECTOR('',#30540,1000.);
#7976=VECTOR('',#30543,1000.);
#7977=VECTOR('',#30544,1000.);
#7978=VECTOR('',#30545,1000.);
#7979=VECTOR('',#30548,1000.);
#7980=VECTOR('',#30549,1000.);
#7981=VECTOR('',#30550,1000.);
#7982=VECTOR('',#30553,1000.);
#7983=VECTOR('',#30554,1000.);
#9684=CIRCLE('',#26018,2.99999999999999);
#9685=CIRCLE('',#26019,2.99999999999999);
#9686=CIRCLE('',#26021,2.99999999999999);
#9687=CIRCLE('',#26022,2.99999999999999);
#9688=CIRCLE('',#26024,3.3);
#9689=CIRCLE('',#26025,3.3);
#9690=CIRCLE('',#26027,3.3);
#9691=CIRCLE('',#26028,3.3);
#9692=CIRCLE('',#26030,3.3);
#9693=CIRCLE('',#26031,3.3);
#9694=CIRCLE('',#26033,3.3);
#9695=CIRCLE('',#26034,3.3);
#11249=VERTEX_POINT('',#52861);
#11250=VERTEX_POINT('',#52863);
#11251=VERTEX_POINT('',#52867);
#11252=VERTEX_POINT('',#52869);
#11253=VERTEX_POINT('',#52873);
#11254=VERTEX_POINT('',#52875);
#11255=VERTEX_POINT('',#52879);
#11256=VERTEX_POINT('',#52881);
#11257=VERTEX_POINT('',#52885);
#11258=VERTEX_POINT('',#52887);
#11259=VERTEX_POINT('',#52891);
#11260=VERTEX_POINT('',#52893);
#11261=VERTEX_POINT('',#52897);
#11262=VERTEX_POINT('',#52898);
#11263=VERTEX_POINT('',#52900);
#11264=VERTEX_POINT('',#52902);
#11265=VERTEX_POINT('',#52906);
#11266=VERTEX_POINT('',#52908);
#11267=VERTEX_POINT('',#52912);
#11268=VERTEX_POINT('',#52914);
#14021=EDGE_CURVE('',#11249,#11249,#9684,.T.);
#14022=EDGE_CURVE('',#11249,#11250,#5999,.T.);
#14023=EDGE_CURVE('',#11250,#11250,#9685,.T.);
#14024=EDGE_CURVE('',#11251,#11251,#9686,.T.);
#14025=EDGE_CURVE('',#11251,#11252,#6000,.T.);
#14026=EDGE_CURVE('',#11252,#11252,#9687,.T.);
#14027=EDGE_CURVE('',#11253,#11253,#9688,.T.);
#14028=EDGE_CURVE('',#11253,#11254,#6001,.T.);
#14029=EDGE_CURVE('',#11254,#11254,#9689,.T.);
#14030=EDGE_CURVE('',#11255,#11255,#9690,.T.);
#14031=EDGE_CURVE('',#11255,#11256,#6002,.T.);
#14032=EDGE_CURVE('',#11256,#11256,#9691,.T.);
#14033=EDGE_CURVE('',#11257,#11257,#9692,.T.);
#14034=EDGE_CURVE('',#11257,#11258,#6003,.T.);
#14035=EDGE_CURVE('',#11258,#11258,#9693,.T.);
#14036=EDGE_CURVE('',#11259,#11259,#9694,.T.);
#14037=EDGE_CURVE('',#11259,#11260,#6004,.T.);
#14038=EDGE_CURVE('',#11260,#11260,#9695,.T.);
#14039=EDGE_CURVE('',#11261,#11262,#6005,.T.);
#14040=EDGE_CURVE('',#11263,#11262,#6006,.T.);
#14041=EDGE_CURVE('',#11264,#11263,#6007,.T.);
#14042=EDGE_CURVE('',#11264,#11261,#6008,.T.);
#14043=EDGE_CURVE('',#11262,#11265,#6009,.T.);
#14044=EDGE_CURVE('',#11266,#11265,#6010,.T.);
#14045=EDGE_CURVE('',#11263,#11266,#6011,.T.);
#14046=EDGE_CURVE('',#11265,#11267,#6012,.T.);
#14047=EDGE_CURVE('',#11268,#11267,#6013,.T.);
#14048=EDGE_CURVE('',#11266,#11268,#6014,.T.);
#14049=EDGE_CURVE('',#11267,#11261,#6015,.T.);
#14050=EDGE_CURVE('',#11268,#11264,#6016,.T.);
#18952=ORIENTED_EDGE('',*,*,#14021,.F.);
#18953=ORIENTED_EDGE('',*,*,#14022,.T.);
#18954=ORIENTED_EDGE('',*,*,#14023,.T.);
#18955=ORIENTED_EDGE('',*,*,#14022,.F.);
#18956=ORIENTED_EDGE('',*,*,#14024,.F.);
#18957=ORIENTED_EDGE('',*,*,#14025,.T.);
#18958=ORIENTED_EDGE('',*,*,#14026,.T.);
#18959=ORIENTED_EDGE('',*,*,#14025,.F.);
#18960=ORIENTED_EDGE('',*,*,#14027,.F.);
#18961=ORIENTED_EDGE('',*,*,#14028,.T.);
#18962=ORIENTED_EDGE('',*,*,#14029,.T.);
#18963=ORIENTED_EDGE('',*,*,#14028,.F.);
#18964=ORIENTED_EDGE('',*,*,#14030,.F.);
#18965=ORIENTED_EDGE('',*,*,#14031,.T.);
#18966=ORIENTED_EDGE('',*,*,#14032,.T.);
#18967=ORIENTED_EDGE('',*,*,#14031,.F.);
#18968=ORIENTED_EDGE('',*,*,#14033,.F.);
#18969=ORIENTED_EDGE('',*,*,#14034,.T.);
#18970=ORIENTED_EDGE('',*,*,#14035,.T.);
#18971=ORIENTED_EDGE('',*,*,#14034,.F.);
#18972=ORIENTED_EDGE('',*,*,#14036,.F.);
#18973=ORIENTED_EDGE('',*,*,#14037,.T.);
#18974=ORIENTED_EDGE('',*,*,#14038,.T.);
#18975=ORIENTED_EDGE('',*,*,#14037,.F.);
#18976=ORIENTED_EDGE('',*,*,#14039,.T.);
#18977=ORIENTED_EDGE('',*,*,#14040,.F.);
#18978=ORIENTED_EDGE('',*,*,#14041,.F.);
#18979=ORIENTED_EDGE('',*,*,#14042,.T.);
#18980=ORIENTED_EDGE('',*,*,#14043,.T.);
#18981=ORIENTED_EDGE('',*,*,#14044,.F.);
#18982=ORIENTED_EDGE('',*,*,#14045,.F.);
#18983=ORIENTED_EDGE('',*,*,#14040,.T.);
#18984=ORIENTED_EDGE('',*,*,#14046,.T.);
#18985=ORIENTED_EDGE('',*,*,#14047,.F.);
#18986=ORIENTED_EDGE('',*,*,#14048,.F.);
#18987=ORIENTED_EDGE('',*,*,#14044,.T.);
#18988=ORIENTED_EDGE('',*,*,#14049,.T.);
#18989=ORIENTED_EDGE('',*,*,#14042,.F.);
#18990=ORIENTED_EDGE('',*,*,#14050,.F.);
#18991=ORIENTED_EDGE('',*,*,#14047,.T.);
#18992=ORIENTED_EDGE('',*,*,#14041,.T.);
#18993=ORIENTED_EDGE('',*,*,#14045,.T.);
#18994=ORIENTED_EDGE('',*,*,#14048,.T.);
#18995=ORIENTED_EDGE('',*,*,#14050,.T.);
#18996=ORIENTED_EDGE('',*,*,#14023,.F.);
#18997=ORIENTED_EDGE('',*,*,#14026,.F.);
#18998=ORIENTED_EDGE('',*,*,#14029,.F.);
#18999=ORIENTED_EDGE('',*,*,#14032,.F.);
#19000=ORIENTED_EDGE('',*,*,#14035,.F.);
#19001=ORIENTED_EDGE('',*,*,#14038,.F.);
#19002=ORIENTED_EDGE('',*,*,#14039,.F.);
#19003=ORIENTED_EDGE('',*,*,#14049,.F.);
#19004=ORIENTED_EDGE('',*,*,#14046,.F.);
#19005=ORIENTED_EDGE('',*,*,#14043,.F.);
#19006=ORIENTED_EDGE('',*,*,#14021,.T.);
#19007=ORIENTED_EDGE('',*,*,#14024,.T.);
#19008=ORIENTED_EDGE('',*,*,#14027,.T.);
#19009=ORIENTED_EDGE('',*,*,#14030,.T.);
#19010=ORIENTED_EDGE('',*,*,#14033,.T.);
#19011=ORIENTED_EDGE('',*,*,#14036,.T.);
#22896=CYLINDRICAL_SURFACE('',#26017,2.99999999999999);
#22897=CYLINDRICAL_SURFACE('',#26020,2.99999999999999);
#22898=CYLINDRICAL_SURFACE('',#26023,3.3);
#22899=CYLINDRICAL_SURFACE('',#26026,3.3);
#22900=CYLINDRICAL_SURFACE('',#26029,3.3);
#22901=CYLINDRICAL_SURFACE('',#26032,3.3);
#23794=ADVANCED_FACE('',(#2802),#22896,.F.);
#23795=ADVANCED_FACE('',(#2803),#22897,.F.);
#23796=ADVANCED_FACE('',(#2804),#22898,.F.);
#23797=ADVANCED_FACE('',(#2805),#22899,.F.);
#23798=ADVANCED_FACE('',(#2806),#22900,.F.);
#23799=ADVANCED_FACE('',(#2807),#22901,.F.);
#23800=ADVANCED_FACE('',(#2808),#1668,.F.);
#23801=ADVANCED_FACE('',(#2809),#1669,.F.);
#23802=ADVANCED_FACE('',(#2810),#1670,.F.);
#23803=ADVANCED_FACE('',(#2811),#1671,.F.);
#23804=ADVANCED_FACE('',(#2812,#1171,#1172,#1173,#1174,#1175,#1176),#1672,
 .T.);
#23805=ADVANCED_FACE('',(#2813,#1177,#1178,#1179,#1180,#1181,#1182),#1673,
 .F.);
#24545=CLOSED_SHELL('',(#23794,#23795,#23796,#23797,#23798,#23799,#23800,
#23801,#23802,#23803,#23804,#23805));
#26016=AXIS2_PLACEMENT_3D('',#52859,#30491,#30492);
#26017=AXIS2_PLACEMENT_3D('',#52860,#30493,#30494);
#26018=AXIS2_PLACEMENT_3D('',#52862,#30495,#30496);
#26019=AXIS2_PLACEMENT_3D('',#52865,#30498,#30499);
#26020=AXIS2_PLACEMENT_3D('',#52866,#30500,#30501);
#26021=AXIS2_PLACEMENT_3D('',#52868,#30502,#30503);
#26022=AXIS2_PLACEMENT_3D('',#52871,#30505,#30506);
#26023=AXIS2_PLACEMENT_3D('',#52872,#30507,#30508);
#26024=AXIS2_PLACEMENT_3D('',#52874,#30509,#30510);
#26025=AXIS2_PLACEMENT_3D('',#52877,#30512,#30513);
#26026=AXIS2_PLACEMENT_3D('',#52878,#30514,#30515);
#26027=AXIS2_PLACEMENT_3D('',#52880,#30516,#30517);
#26028=AXIS2_PLACEMENT_3D('',#52883,#30519,#30520);
#26029=AXIS2_PLACEMENT_3D('',#52884,#30521,#30522);
#26030=AXIS2_PLACEMENT_3D('',#52886,#30523,#30524);
#26031=AXIS2_PLACEMENT_3D('',#52889,#30526,#30527);
#26032=AXIS2_PLACEMENT_3D('',#52890,#30528,#30529);
#26033=AXIS2_PLACEMENT_3D('',#52892,#30530,#30531);
#26034=AXIS2_PLACEMENT_3D('',#52895,#30533,#30534);
#26035=AXIS2_PLACEMENT_3D('',#52896,#30535,#30536);
#26036=AXIS2_PLACEMENT_3D('',#52905,#30541,#30542);
#26037=AXIS2_PLACEMENT_3D('',#52911,#30546,#30547);
#26038=AXIS2_PLACEMENT_3D('',#52917,#30551,#30552);
#26039=AXIS2_PLACEMENT_3D('',#52920,#30555,#30556);
#26040=AXIS2_PLACEMENT_3D('',#52921,#30557,#30558);
#30491=DIRECTION('axis',(0.,0.,1.));
#30492=DIRECTION('refdir',(1.,0.,0.));
#30493=DIRECTION('center_axis',(0.,0.,1.));
#30494=DIRECTION('ref_axis',(1.,0.,0.));
#30495=DIRECTION('center_axis',(0.,0.,1.));
#30496=DIRECTION('ref_axis',(1.,0.,0.));
#30497=DIRECTION('',(0.,0.,1.));
#30498=DIRECTION('center_axis',(0.,0.,1.));
#30499=DIRECTION('ref_axis',(1.,0.,0.));
#30500=DIRECTION('center_axis',(0.,0.,1.));
#30501=DIRECTION('ref_axis',(1.,0.,0.));
#30502=DIRECTION('center_axis',(0.,0.,1.));
#30503=DIRECTION('ref_axis',(1.,0.,0.));
#30504=DIRECTION('',(0.,0.,1.));
#30505=DIRECTION('center_axis',(0.,0.,1.));
#30506=DIRECTION('ref_axis',(1.,0.,0.));
#30507=DIRECTION('center_axis',(0.,0.,1.));
#30508=DIRECTION('ref_axis',(1.,0.,0.));
#30509=DIRECTION('center_axis',(0.,0.,1.));
#30510=DIRECTION('ref_axis',(1.,0.,0.));
#30511=DIRECTION('',(0.,0.,1.));
#30512=DIRECTION('center_axis',(0.,0.,1.));
#30513=DIRECTION('ref_axis',(1.,0.,0.));
#30514=DIRECTION('center_axis',(0.,0.,1.));
#30515=DIRECTION('ref_axis',(1.,0.,0.));
#30516=DIRECTION('center_axis',(0.,0.,1.));
#30517=DIRECTION('ref_axis',(1.,0.,0.));
#30518=DIRECTION('',(0.,0.,1.));
#30519=DIRECTION('center_axis',(0.,0.,1.));
#30520=DIRECTION('ref_axis',(1.,0.,0.));
#30521=DIRECTION('center_axis',(0.,0.,1.));
#30522=DIRECTION('ref_axis',(1.,0.,0.));
#30523=DIRECTION('center_axis',(0.,0.,1.));
#30524=DIRECTION('ref_axis',(1.,0.,0.));
#30525=DIRECTION('',(0.,0.,1.));
#30526=DIRECTION('center_axis',(0.,0.,1.));
#30527=DIRECTION('ref_axis',(1.,0.,0.));
#30528=DIRECTION('center_axis',(0.,0.,1.));
#30529=DIRECTION('ref_axis',(1.,0.,0.));
#30530=DIRECTION('center_axis',(0.,0.,1.));
#30531=DIRECTION('ref_axis',(1.,0.,0.));
#30532=DIRECTION('',(0.,0.,1.));
#30533=DIRECTION('center_axis',(0.,0.,1.));
#30534=DIRECTION('ref_axis',(1.,0.,0.));
#30535=DIRECTION('center_axis',(-1.,-9.25185853854297E-17,0.));
#30536=DIRECTION('ref_axis',(9.25185853854297E-17,-1.,0.));
#30537=DIRECTION('',(-9.25185853854297E-17,1.,0.));
#30538=DIRECTION('',(0.,0.,-1.));
#30539=DIRECTION('',(-9.25185853854297E-17,1.,0.));
#30540=DIRECTION('',(0.,0.,-1.));
#30541=DIRECTION('center_axis',(0.,-1.,0.));
#30542=DIRECTION('ref_axis',(0.,0.,-1.));
#30543=DIRECTION('',(-1.,0.,0.));
#30544=DIRECTION('',(0.,0.,-1.));
#30545=DIRECTION('',(-1.,0.,0.));
#30546=DIRECTION('center_axis',(1.,1.85037170770859E-16,0.));
#30547=DIRECTION('ref_axis',(-1.85037170770859E-16,1.,0.));
#30548=DIRECTION('',(1.85037170770859E-16,-1.,0.));
#30549=DIRECTION('',(0.,0.,-1.));
#30550=DIRECTION('',(1.85037170770859E-16,-1.,0.));
#30551=DIRECTION('center_axis',(0.,1.,0.));
#30552=DIRECTION('ref_axis',(0.,0.,1.));
#30553=DIRECTION('',(1.,0.,0.));
#30554=DIRECTION('',(1.,0.,0.));
#30555=DIRECTION('center_axis',(0.,0.,1.));
#30556=DIRECTION('ref_axis',(1.,0.,0.));
#30557=DIRECTION('center_axis',(0.,0.,1.));
#30558=DIRECTION('ref_axis',(1.,0.,0.));
#52859=CARTESIAN_POINT('',(0.,0.,0.));
#52860=CARTESIAN_POINT('Origin',(-14.,25.,5.));
#52861=CARTESIAN_POINT('',(-17.,25.,-5.));
#52862=CARTESIAN_POINT('Origin',(-14.,25.,-5.));
#52863=CARTESIAN_POINT('',(-17.,25.,5.));
#52864=CARTESIAN_POINT('',(-17.,25.,5.));
#52865=CARTESIAN_POINT('Origin',(-14.,25.,5.));
#52866=CARTESIAN_POINT('Origin',(14.,-25.,5.));
#52867=CARTESIAN_POINT('',(11.,-25.,-5.));
#52868=CARTESIAN_POINT('Origin',(14.,-25.,-5.));
#52869=CARTESIAN_POINT('',(11.,-25.,5.));
#52870=CARTESIAN_POINT('',(11.,-25.,5.));
#52871=CARTESIAN_POINT('Origin',(14.,-25.,5.));
#52872=CARTESIAN_POINT('Origin',(34.,25.,5.));
#52873=CARTESIAN_POINT('',(30.7,25.,-5.));
#52874=CARTESIAN_POINT('Origin',(34.,25.,-5.));
#52875=CARTESIAN_POINT('',(30.7,25.,5.));
#52876=CARTESIAN_POINT('',(30.7,25.,5.));
#52877=CARTESIAN_POINT('Origin',(34.,25.,5.));
#52878=CARTESIAN_POINT('Origin',(-34.,25.,5.));
#52879=CARTESIAN_POINT('',(-37.3,25.,-5.));
#52880=CARTESIAN_POINT('Origin',(-34.,25.,-5.));
#52881=CARTESIAN_POINT('',(-37.3,25.,5.));
#52882=CARTESIAN_POINT('',(-37.3,25.,5.));
#52883=CARTESIAN_POINT('Origin',(-34.,25.,5.));
#52884=CARTESIAN_POINT('Origin',(-34.,-25.,5.));
#52885=CARTESIAN_POINT('',(-37.3,-25.,-5.));
#52886=CARTESIAN_POINT('Origin',(-34.,-25.,-5.));
#52887=CARTESIAN_POINT('',(-37.3,-25.,5.));
#52888=CARTESIAN_POINT('',(-37.3,-25.,5.));
#52889=CARTESIAN_POINT('Origin',(-34.,-25.,5.));
#52890=CARTESIAN_POINT('Origin',(34.,-25.,5.));
#52891=CARTESIAN_POINT('',(30.7,-25.,-5.));
#52892=CARTESIAN_POINT('Origin',(34.,-25.,-5.));
#52893=CARTESIAN_POINT('',(30.7,-25.,5.));
#52894=CARTESIAN_POINT('',(30.7,-25.,5.));
#52895=CARTESIAN_POINT('Origin',(34.,-25.,5.));
#52896=CARTESIAN_POINT('Origin',(47.5,37.5,5.));
#52897=CARTESIAN_POINT('',(47.5,-37.5,-5.));
#52898=CARTESIAN_POINT('',(47.5,37.5,-5.));
#52899=CARTESIAN_POINT('',(47.5,37.5,-5.));
#52900=CARTESIAN_POINT('',(47.5,37.5,5.));
#52901=CARTESIAN_POINT('',(47.5,37.5,5.));
#52902=CARTESIAN_POINT('',(47.5,-37.5,5.));
#52903=CARTESIAN_POINT('',(47.5,37.5,5.));
#52904=CARTESIAN_POINT('',(47.5,-37.5,5.));
#52905=CARTESIAN_POINT('Origin',(-47.5,37.5,5.));
#52906=CARTESIAN_POINT('',(-47.5,37.5,-5.));
#52907=CARTESIAN_POINT('',(-47.5,37.5,-5.));
#52908=CARTESIAN_POINT('',(-47.5,37.5,5.));
#52909=CARTESIAN_POINT('',(-47.5,37.5,5.));
#52910=CARTESIAN_POINT('',(-47.5,37.5,5.));
#52911=CARTESIAN_POINT('Origin',(-47.5,37.5,5.));
#52912=CARTESIAN_POINT('',(-47.5,-37.5,-5.));
#52913=CARTESIAN_POINT('',(-47.5,37.5,-5.));
#52914=CARTESIAN_POINT('',(-47.5,-37.5,5.));
#52915=CARTESIAN_POINT('',(-47.5,-37.5,5.));
#52916=CARTESIAN_POINT('',(-47.5,37.5,5.));
#52917=CARTESIAN_POINT('Origin',(-47.5,-37.5,5.));
#52918=CARTESIAN_POINT('',(-47.5,-37.5,-5.));
#52919=CARTESIAN_POINT('',(-47.5,-37.5,5.));
#52920=CARTESIAN_POINT('Origin',(0.,0.,5.));
#52921=CARTESIAN_POINT('Origin',(0.,0.,-5.));
#57027=UNCERTAINTY_MEASURE_WITH_UNIT(LENGTH_MEASURE(0.01),#57080,
'DISTANCE_ACCURACY_VALUE',
'Maximum model space distance between geometric entities at asserted c
onnectivities');
#57040=UNCERTAINTY_MEASURE_WITH_UNIT(LENGTH_MEASURE(0.01),#57080,
'DISTANCE_ACCURACY_VALUE',
'Maximum model space distance between geometric entities at asserted c
onnectivities');
#57066=(
GEOMETRIC_REPRESENTATION_CONTEXT(3)
GLOBAL_UNCERTAINTY_ASSIGNED_CONTEXT((#57027))
GLOBAL_UNIT_ASSIGNED_CONTEXT((#57080,#57082,#57083))
REPRESENTATION_CONTEXT('','3D')
);
#57079=(
GEOMETRIC_REPRESENTATION_CONTEXT(3)
GLOBAL_UNCERTAINTY_ASSIGNED_CONTEXT((#57040))
GLOBAL_UNIT_ASSIGNED_CONTEXT((#57080,#57082,#57083))
REPRESENTATION_CONTEXT('','3D')
);
#57080=(
LENGTH_UNIT()
NAMED_UNIT(*)
SI_UNIT(.MILLI.,.METRE.)
);
#57082=(
NAMED_UNIT(*)
PLANE_ANGLE_UNIT()
SI_UNIT($,.RADIAN.)
);
#57083=(
NAMED_UNIT(*)
SI_UNIT($,.STERADIAN.)
SOLID_ANGLE_UNIT()
);
#57109=SHAPE_DEFINITION_REPRESENTATION(#57161,#57274);
#57161=PRODUCT_DEFINITION_SHAPE('',$,#57313);
#57274=SHAPE_REPRESENTATION('',(#26016),#57066);
#57287=PRODUCT_DEFINITION_CONTEXT('part definition',#57403,'design');
#57313=PRODUCT_DEFINITION('Ball Screw Support Plate',
'Ball Screw Support Plate',#57351,#57287);
#57351=PRODUCT_DEFINITION_FORMATION('',$,#57430);
#57403=APPLICATION_CONTEXT(
'Core Data for Automotive Mechanical Design Process');
#57404=PRODUCT_CONTEXT('part definition',#57403,'mechanical');
#57430=PRODUCT('Ball Screw Support Plate','Ball Screw Support Plate',$,
(#57404));
#57444=PRESENTATION_STYLE_ASSIGNMENT((#57446));
#57446=SURFACE_STYLE_USAGE(.BOTH.,#57448);
#57448=SURFACE_SIDE_STYLE('',(#57450));
#57450=SURFACE_STYLE_FILL_AREA(#57452);
#57452=FILL_AREA_STYLE('Opaque(202,209,238)',(#57454));
#57454=FILL_AREA_STYLE_COLOUR('Opaque(202,209,238)',#57456);
#57456=COLOUR_RGB('Opaque(202,209,238)',0.792156862745098,0.819607843137255,
0.933333333333333);
ENDSEC;
END-ISO-10303-21;
